ISO-10303-21;
HEADER;
/* Generated by software containing ST-Developer
 * from STEP Tools, Inc. (www.steptools.com) 
 */

FILE_DESCRIPTION(
/* description */ ('Single-Axis Profile-Rail Linear Slide'),
/* implementation_level */ '2;1');

FILE_NAME(
/* name */ 'Flat Washer - M5.step',
/* time_stamp */ '2026-10-27T10:47:43-07:00',
/* author */ (''),
/* organization */ (''),
/* preprocessor_version */ 'ST-DEVELOPER v20.2',
/* originating_system */ 'Autodesk Translation Framework v15.17.0.0',
/* authorisation */ '');

FILE_SCHEMA (('AUTOMOTIVE_DESIGN { 1 0 10303 214 3 1 1 }'));
ENDSEC;

DATA;
#10=MECHANICAL_DESIGN_GEOMETRIC_PRESENTATION_REPRESENTATION('',(#350),#14478);
#249=CONICAL_SURFACE('',#9458,0.275,0.785398163397449);
#296=SHAPE_REPRESENTATION_RELATIONSHIP('SRR','None',#14628,#323);
#323=ADVANCED_BREP_SHAPE_REPRESENTATION('',(#375),#14472);
#350=STYLED_ITEM('',(#14838),#375);
#375=MANIFOLD_SOLID_BREP('Body1',#8612);
#459=FACE_BOUND('',#1769,.T.);
#460=FACE_BOUND('',#1772,.T.);
#801=PLANE('',#9463);
#802=PLANE('',#9467);
#1230=FACE_OUTER_BOUND('',#1766,.T.);
#1231=FACE_OUTER_BOUND('',#1767,.T.);
#1232=FACE_OUTER_BOUND('',#1768,.T.);
#1233=FACE_OUTER_BOUND('',#1770,.T.);
#1234=FACE_OUTER_BOUND('',#1771,.T.);
#1766=EDGE_LOOP('',(#7835,#7836,#7837,#7838));
#1767=EDGE_LOOP('',(#7839,#7840,#7841,#7842));
#1768=EDGE_LOOP('',(#7843));
#1769=EDGE_LOOP('',(#7844));
#1770=EDGE_LOOP('',(#7845,#7846,#7847,#7848));
#1771=EDGE_LOOP('',(#7849));
#1772=EDGE_LOOP('',(#7850));
#2731=LINE('',#14102,#3702);
#2732=LINE('',#14106,#3703);
#2733=LINE('',#14113,#3704);
#3702=VECTOR('',#11594,0.275);
#3703=VECTOR('',#11599,0.265);
#3704=VECTOR('',#11608,0.5);
#3900=CIRCLE('',#9459,0.285);
#3901=CIRCLE('',#9460,0.265);
#3902=CIRCLE('',#9462,0.265);
#3903=CIRCLE('',#9464,0.5);
#3904=CIRCLE('',#9466,0.5);
#4610=VERTEX_POINT('',#14099);
#4611=VERTEX_POINT('',#14101);
#4612=VERTEX_POINT('',#14105);
#4613=VERTEX_POINT('',#14109);
#4614=VERTEX_POINT('',#14112);
#5695=EDGE_CURVE('',#4610,#4610,#3900,.T.);
#5696=EDGE_CURVE('',#4610,#4611,#2731,.T.);
#5697=EDGE_CURVE('',#4611,#4611,#3901,.T.);
#5698=EDGE_CURVE('',#4611,#4612,#2732,.T.);
#5699=EDGE_CURVE('',#4612,#4612,#3902,.T.);
#5700=EDGE_CURVE('',#4613,#4613,#3903,.T.);
#5701=EDGE_CURVE('',#4613,#4614,#2733,.T.);
#5702=EDGE_CURVE('',#4614,#4614,#3904,.T.);
#7835=ORIENTED_EDGE('',*,*,#5695,.T.);
#7836=ORIENTED_EDGE('',*,*,#5696,.T.);
#7837=ORIENTED_EDGE('',*,*,#5697,.T.);
#7838=ORIENTED_EDGE('',*,*,#5696,.F.);
#7839=ORIENTED_EDGE('',*,*,#5697,.F.);
#7840=ORIENTED_EDGE('',*,*,#5698,.T.);
#7841=ORIENTED_EDGE('',*,*,#5699,.T.);
#7842=ORIENTED_EDGE('',*,*,#5698,.F.);
#7843=ORIENTED_EDGE('',*,*,#5700,.T.);
#7844=ORIENTED_EDGE('',*,*,#5695,.F.);
#7845=ORIENTED_EDGE('',*,*,#5700,.F.);
#7846=ORIENTED_EDGE('',*,*,#5701,.T.);
#7847=ORIENTED_EDGE('',*,*,#5702,.T.);
#7848=ORIENTED_EDGE('',*,*,#5701,.F.);
#7849=ORIENTED_EDGE('',*,*,#5702,.F.);
#7850=ORIENTED_EDGE('',*,*,#5699,.F.);
#8122=CYLINDRICAL_SURFACE('',#9461,0.265);
#8123=CYLINDRICAL_SURFACE('',#9465,0.5);
#8524=ADVANCED_FACE('',(#1230),#249,.F.);
#8525=ADVANCED_FACE('',(#1231),#8122,.F.);
#8526=ADVANCED_FACE('',(#1232,#459),#801,.T.);
#8527=ADVANCED_FACE('',(#1233),#8123,.T.);
#8528=ADVANCED_FACE('',(#1234,#460),#802,.F.);
#8612=CLOSED_SHELL('',(#8524,#8525,#8526,#8527,#8528));
#9457=AXIS2_PLACEMENT_3D('',#14097,#11588,#11589);
#9458=AXIS2_PLACEMENT_3D('',#14098,#11590,#11591);
#9459=AXIS2_PLACEMENT_3D('',#14100,#11592,#11593);
#9460=AXIS2_PLACEMENT_3D('',#14103,#11595,#11596);
#9461=AXIS2_PLACEMENT_3D('',#14104,#11597,#11598);
#9462=AXIS2_PLACEMENT_3D('',#14107,#11600,#11601);
#9463=AXIS2_PLACEMENT_3D('',#14108,#11602,#11603);
#9464=AXIS2_PLACEMENT_3D('',#14110,#11604,#11605);
#9465=AXIS2_PLACEMENT_3D('',#14111,#11606,#11607);
#9466=AXIS2_PLACEMENT_3D('',#14114,#11609,#11610);
#9467=AXIS2_PLACEMENT_3D('',#14115,#11611,#11612);
#11588=DIRECTION('axis',(0.,0.,1.));
#11589=DIRECTION('refdir',(1.,0.,0.));
#11590=DIRECTION('center_axis',(0.,1.,0.));
#11591=DIRECTION('ref_axis',(1.,0.,0.));
#11592=DIRECTION('center_axis',(0.,1.,0.));
#11593=DIRECTION('ref_axis',(1.,0.,0.));
#11594=DIRECTION('',(0.707106781186548,-0.707106781186547,-8.65956056235494E-17));
#11595=DIRECTION('center_axis',(0.,-1.,0.));
#11596=DIRECTION('ref_axis',(1.,0.,0.));
#11597=DIRECTION('center_axis',(0.,1.,0.));
#11598=DIRECTION('ref_axis',(1.,0.,0.));
#11599=DIRECTION('',(0.,-1.,0.));
#11600=DIRECTION('center_axis',(0.,-1.,0.));
#11601=DIRECTION('ref_axis',(1.,0.,0.));
#11602=DIRECTION('center_axis',(0.,1.,0.));
#11603=DIRECTION('ref_axis',(1.,0.,0.));
#11604=DIRECTION('center_axis',(0.,1.,0.));
#11605=DIRECTION('ref_axis',(1.,0.,0.));
#11606=DIRECTION('center_axis',(0.,1.,0.));
#11607=DIRECTION('ref_axis',(1.,0.,0.));
#11608=DIRECTION('',(0.,-1.,0.));
#11609=DIRECTION('center_axis',(0.,1.,0.));
#11610=DIRECTION('ref_axis',(1.,0.,0.));
#11611=DIRECTION('center_axis',(0.,1.,0.));
#11612=DIRECTION('ref_axis',(1.,0.,0.));
#14097=CARTESIAN_POINT('',(0.,0.,0.));
#14098=CARTESIAN_POINT('Origin',(0.,0.09,0.));
#14099=CARTESIAN_POINT('',(-0.285,0.1,3.49024337756996E-17));
#14100=CARTESIAN_POINT('Origin',(0.,0.1,0.));
#14101=CARTESIAN_POINT('',(-0.265,0.08,-3.24531401774049E-17));
#14102=CARTESIAN_POINT('',(-0.275,0.09,3.36777869765522E-17));
#14103=CARTESIAN_POINT('Origin',(0.,0.08,0.));
#14104=CARTESIAN_POINT('Origin',(0.,0.,0.));
#14105=CARTESIAN_POINT('',(-0.265,0.,3.24531401774049E-17));
#14106=CARTESIAN_POINT('',(-0.265,0.,3.24531401774049E-17));
#14107=CARTESIAN_POINT('Origin',(0.,0.,0.));
#14108=CARTESIAN_POINT('Origin',(0.,0.1,0.));
#14109=CARTESIAN_POINT('',(-0.5,0.1,6.12323399573677E-17));
#14110=CARTESIAN_POINT('Origin',(0.,0.1,0.));
#14111=CARTESIAN_POINT('Origin',(0.,0.,0.));
#14112=CARTESIAN_POINT('',(-0.5,0.,6.12323399573677E-17));
#14113=CARTESIAN_POINT('',(-0.5,0.,6.12323399573677E-17));
#14114=CARTESIAN_POINT('Origin',(0.,0.,0.));
#14115=CARTESIAN_POINT('Origin',(0.,0.,0.));
#14440=UNCERTAINTY_MEASURE_WITH_UNIT(LENGTH_MEASURE(0.001),#14479,
'DISTANCE_ACCURACY_VALUE',
'Maximum model space distance between geometric entities at asserted c
onnectivities');
#14446=UNCERTAINTY_MEASURE_WITH_UNIT(LENGTH_MEASURE(0.001),#14479,
'DISTANCE_ACCURACY_VALUE',
'Maximum model space distance between geometric entities at asserted c
onnectivities');
#14472=(
GEOMETRIC_REPRESENTATION_CONTEXT(3)
GLOBAL_UNCERTAINTY_ASSIGNED_CONTEXT((#14440))
GLOBAL_UNIT_ASSIGNED_CONTEXT((#14479,#14481,#14482))
REPRESENTATION_CONTEXT('','3D')
);
#14478=(
GEOMETRIC_REPRESENTATION_CONTEXT(3)
GLOBAL_UNCERTAINTY_ASSIGNED_CONTEXT((#14446))
GLOBAL_UNIT_ASSIGNED_CONTEXT((#14479,#14481,#14482))
REPRESENTATION_CONTEXT('','3D')
);
#14479=(
LENGTH_UNIT()
NAMED_UNIT(*)
SI_UNIT(.CENTI.,.METRE.)
);
#14481=(
NAMED_UNIT(*)
PLANE_ANGLE_UNIT()
SI_UNIT($,.RADIAN.)
);
#14482=(
NAMED_UNIT(*)
SI_UNIT($,.STERADIAN.)
SOLID_ANGLE_UNIT()
);
#14508=SHAPE_DEFINITION_REPRESENTATION(#14542,#14628);
#14542=PRODUCT_DEFINITION_SHAPE('',$,#14660);
#14628=SHAPE_REPRESENTATION('',(#9457),#14472);
#14634=PRODUCT_DEFINITION_CONTEXT('part definition',#14729,'design');
#14660=PRODUCT_DEFINITION('Flat Washer - M5','Flat Washer - M5',#14691,
#14634);
#14691=PRODUCT_DEFINITION_FORMATION('',$,#14756);
#14729=APPLICATION_CONTEXT(
'Core Data for Automotive Mechanical Design Process');
#14730=PRODUCT_CONTEXT('part definition',#14729,'mechanical');
#14756=PRODUCT('Flat Washer - M5','Flat Washer - M5','Flat Washer - M5',
(#14730));
#14832=COLOUR_RGB('Black',0.12,0.14,0.17);
#14833=FILL_AREA_STYLE_COLOUR('',#14832);
#14834=FILL_AREA_STYLE('',(#14833));
#14835=SURFACE_STYLE_FILL_AREA(#14834);
#14836=SURFACE_SIDE_STYLE('',(#14835));
#14837=SURFACE_STYLE_USAGE(.BOTH.,#14836);
#14838=PRESENTATION_STYLE_ASSIGNMENT((#14837));
ENDSEC;
END-ISO-10303-21;
